ISO-10303-21;
HEADER;
/* Generated by software containing ST-Developer
 * from STEP Tools, Inc. (www.steptools.com) 
 */

FILE_DESCRIPTION(
/* description */ ('Single-Axis Profile-Rail Linear Slide'),
/* implementation_level */ '2;1');

FILE_NAME(
/* name */ 'Captive slot nut.step',
/* time_stamp */ '2026-10-27T10:47:43-07:00',
/* author */ (''),
/* organization */ (''),
/* preprocessor_version */ 'ST-DEVELOPER v20.2',
/* originating_system */ 'Autodesk Translation Framework v15.17.0.0',
/* authorisation */ '');

FILE_SCHEMA (('AUTOMOTIVE_DESIGN { 1 0 10303 214 3 1 1 }'));
ENDSEC;

DATA;
#10=MECHANICAL_DESIGN_GEOMETRIC_PRESENTATION_REPRESENTATION('',(#341),#14478);
#273=ELLIPSE('',#9287,0.299389011154384,0.2117);
#274=ELLIPSE('',#9291,0.299389011154384,0.2117);
#287=SHAPE_REPRESENTATION_RELATIONSHIP('SRR','None',#14617,#314);
#314=ADVANCED_BREP_SHAPE_REPRESENTATION('',(#368),#14461);
#341=STYLED_ITEM('',(#14838),#368);
#368=MANIFOLD_SOLID_BREP('Body1',#8601);
#436=FACE_BOUND('',#1633,.T.);
#712=PLANE('',#9277);
#713=PLANE('',#9278);
#714=PLANE('',#9279);
#715=PLANE('',#9281);
#716=PLANE('',#9282);
#717=PLANE('',#9283);
#718=PLANE('',#9284);
#719=PLANE('',#9285);
#720=PLANE('',#9286);
#721=PLANE('',#9293);
#722=PLANE('',#9294);
#723=PLANE('',#9295);
#724=PLANE('',#9296);
#1117=FACE_OUTER_BOUND('',#1630,.T.);
#1118=FACE_OUTER_BOUND('',#1631,.T.);
#1119=FACE_OUTER_BOUND('',#1632,.T.);
#1120=FACE_OUTER_BOUND('',#1634,.T.);
#1121=FACE_OUTER_BOUND('',#1635,.T.);
#1122=FACE_OUTER_BOUND('',#1636,.T.);
#1123=FACE_OUTER_BOUND('',#1637,.T.);
#1124=FACE_OUTER_BOUND('',#1638,.T.);
#1125=FACE_OUTER_BOUND('',#1639,.T.);
#1126=FACE_OUTER_BOUND('',#1640,.T.);
#1127=FACE_OUTER_BOUND('',#1641,.T.);
#1128=FACE_OUTER_BOUND('',#1642,.T.);
#1129=FACE_OUTER_BOUND('',#1643,.T.);
#1130=FACE_OUTER_BOUND('',#1644,.T.);
#1630=EDGE_LOOP('',(#7283,#7284,#7285,#7286));
#1631=EDGE_LOOP('',(#7287,#7288,#7289,#7290));
#1632=EDGE_LOOP('',(#7291,#7292,#7293,#7294));
#1633=EDGE_LOOP('',(#7295));
#1634=EDGE_LOOP('',(#7296,#7297,#7298,#7299,#7300,#7301,#7302,#7303,#7304,
#7305));
#1635=EDGE_LOOP('',(#7306,#7307,#7308,#7309));
#1636=EDGE_LOOP('',(#7310,#7311,#7312,#7313));
#1637=EDGE_LOOP('',(#7314,#7315,#7316,#7317,#7318,#7319,#7320,#7321,#7322,
#7323));
#1638=EDGE_LOOP('',(#7324,#7325,#7326,#7327));
#1639=EDGE_LOOP('',(#7328,#7329,#7330,#7331,#7332,#7333));
#1640=EDGE_LOOP('',(#7334,#7335,#7336,#7337,#7338,#7339,#7340,#7341));
#1641=EDGE_LOOP('',(#7342,#7343,#7344,#7345,#7346));
#1642=EDGE_LOOP('',(#7347,#7348,#7349,#7350));
#1643=EDGE_LOOP('',(#7351,#7352,#7353,#7354,#7355,#7356));
#1644=EDGE_LOOP('',(#7357,#7358,#7359,#7360));
#2509=LINE('',#13516,#3480);
#2510=LINE('',#13518,#3481);
#2511=LINE('',#13520,#3482);
#2512=LINE('',#13521,#3483);
#2513=LINE('',#13524,#3484);
#2514=LINE('',#13526,#3485);
#2515=LINE('',#13527,#3486);
#2516=LINE('',#13530,#3487);
#2517=LINE('',#13532,#3488);
#2518=LINE('',#13533,#3489);
#2519=LINE('',#13538,#3490);
#2520=LINE('',#13540,#3491);
#2521=LINE('',#13542,#3492);
#2522=LINE('',#13544,#3493);
#2523=LINE('',#13546,#3494);
#2524=LINE('',#13548,#3495);
#2525=LINE('',#13549,#3496);
#2526=LINE('',#13552,#3497);
#2527=LINE('',#13553,#3498);
#2528=LINE('',#13556,#3499);
#2529=LINE('',#13557,#3500);
#2530=LINE('',#13560,#3501);
#2531=LINE('',#13562,#3502);
#2532=LINE('',#13564,#3503);
#2533=LINE('',#13566,#3504);
#2534=LINE('',#13567,#3505);
#2535=LINE('',#13569,#3506);
#2536=LINE('',#13572,#3507);
#2537=LINE('',#13575,#3508);
#2538=LINE('',#13579,#3509);
#2539=LINE('',#13586,#3510);
#2540=LINE('',#13588,#3511);
#2541=LINE('',#13590,#3512);
#3480=VECTOR('',#11008,1.);
#3481=VECTOR('',#11009,1.);
#3482=VECTOR('',#11010,1.);
#3483=VECTOR('',#11011,1.);
#3484=VECTOR('',#11014,1.);
#3485=VECTOR('',#11015,1.);
#3486=VECTOR('',#11016,1.);
#3487=VECTOR('',#11019,1.);
#3488=VECTOR('',#11020,1.);
#3489=VECTOR('',#11021,1.);
#3490=VECTOR('',#11026,1.);
#3491=VECTOR('',#11027,1.);
#3492=VECTOR('',#11028,1.);
#3493=VECTOR('',#11029,1.);
#3494=VECTOR('',#11030,1.);
#3495=VECTOR('',#11031,1.);
#3496=VECTOR('',#11032,1.);
#3497=VECTOR('',#11035,1.);
#3498=VECTOR('',#11036,1.);
#3499=VECTOR('',#11039,1.);
#3500=VECTOR('',#11040,1.);
#3501=VECTOR('',#11043,1.);
#3502=VECTOR('',#11044,1.);
#3503=VECTOR('',#11045,1.);
#3504=VECTOR('',#11046,1.);
#3505=VECTOR('',#11047,1.);
#3506=VECTOR('',#11050,1.);
#3507=VECTOR('',#11053,1.);
#3508=VECTOR('',#11056,1.);
#3509=VECTOR('',#11061,0.21);
#3510=VECTOR('',#11070,1.);
#3511=VECTOR('',#11073,1.);
#3512=VECTOR('',#11076,1.);
#3848=CIRCLE('',#9280,0.2117);
#3849=CIRCLE('',#9289,0.2117);
#3850=CIRCLE('',#9290,0.2117);
#3851=CIRCLE('',#9292,0.2117);
#4428=VERTEX_POINT('',#13514);
#4429=VERTEX_POINT('',#13515);
#4430=VERTEX_POINT('',#13517);
#4431=VERTEX_POINT('',#13519);
#4432=VERTEX_POINT('',#13523);
#4433=VERTEX_POINT('',#13525);
#4434=VERTEX_POINT('',#13529);
#4435=VERTEX_POINT('',#13531);
#4436=VERTEX_POINT('',#13534);
#4437=VERTEX_POINT('',#13537);
#4438=VERTEX_POINT('',#13539);
#4439=VERTEX_POINT('',#13541);
#4440=VERTEX_POINT('',#13543);
#4441=VERTEX_POINT('',#13545);
#4442=VERTEX_POINT('',#13547);
#4443=VERTEX_POINT('',#13551);
#4444=VERTEX_POINT('',#13555);
#4445=VERTEX_POINT('',#13559);
#4446=VERTEX_POINT('',#13561);
#4447=VERTEX_POINT('',#13563);
#4448=VERTEX_POINT('',#13565);
#4449=VERTEX_POINT('',#13571);
#4450=VERTEX_POINT('',#13573);
#4451=VERTEX_POINT('',#13577);
#4452=VERTEX_POINT('',#13580);
#4453=VERTEX_POINT('',#13582);
#5419=EDGE_CURVE('',#4428,#4429,#2509,.T.);
#5420=EDGE_CURVE('',#4430,#4428,#2510,.T.);
#5421=EDGE_CURVE('',#4431,#4430,#2511,.T.);
#5422=EDGE_CURVE('',#4429,#4431,#2512,.T.);
#5423=EDGE_CURVE('',#4430,#4432,#2513,.T.);
#5424=EDGE_CURVE('',#4433,#4432,#2514,.T.);
#5425=EDGE_CURVE('',#4431,#4433,#2515,.T.);
#5426=EDGE_CURVE('',#4432,#4434,#2516,.T.);
#5427=EDGE_CURVE('',#4434,#4435,#2517,.T.);
#5428=EDGE_CURVE('',#4435,#4433,#2518,.T.);
#5429=EDGE_CURVE('',#4436,#4436,#3848,.T.);
#5430=EDGE_CURVE('',#4437,#4428,#2519,.T.);
#5431=EDGE_CURVE('',#4438,#4437,#2520,.T.);
#5432=EDGE_CURVE('',#4438,#4439,#2521,.T.);
#5433=EDGE_CURVE('',#4440,#4439,#2522,.T.);
#5434=EDGE_CURVE('',#4440,#4441,#2523,.T.);
#5435=EDGE_CURVE('',#4441,#4442,#2524,.T.);
#5436=EDGE_CURVE('',#4442,#4434,#2525,.T.);
#5437=EDGE_CURVE('',#4442,#4443,#2526,.T.);
#5438=EDGE_CURVE('',#4443,#4435,#2527,.T.);
#5439=EDGE_CURVE('',#4444,#4441,#2528,.T.);
#5440=EDGE_CURVE('',#4443,#4444,#2529,.T.);
#5441=EDGE_CURVE('',#4445,#4444,#2530,.T.);
#5442=EDGE_CURVE('',#4446,#4445,#2531,.T.);
#5443=EDGE_CURVE('',#4446,#4447,#2532,.T.);
#5444=EDGE_CURVE('',#4448,#4447,#2533,.T.);
#5445=EDGE_CURVE('',#4448,#4429,#2534,.T.);
#5446=EDGE_CURVE('',#4445,#4440,#2535,.T.);
#5447=EDGE_CURVE('',#4439,#4449,#2536,.T.);
#5448=EDGE_CURVE('',#4449,#4450,#273,.T.);
#5449=EDGE_CURVE('',#4450,#4446,#2537,.T.);
#5450=EDGE_CURVE('',#4451,#4449,#3849,.F.);
#5451=EDGE_CURVE('',#4451,#4436,#2538,.T.);
#5452=EDGE_CURVE('',#4452,#4451,#3850,.F.);
#5453=EDGE_CURVE('',#4453,#4452,#274,.T.);
#5454=EDGE_CURVE('',#4450,#4453,#3851,.F.);
#5455=EDGE_CURVE('',#4452,#4438,#2539,.T.);
#5456=EDGE_CURVE('',#4447,#4453,#2540,.T.);
#5457=EDGE_CURVE('',#4437,#4448,#2541,.T.);
#7283=ORIENTED_EDGE('',*,*,#5419,.F.);
#7284=ORIENTED_EDGE('',*,*,#5420,.F.);
#7285=ORIENTED_EDGE('',*,*,#5421,.F.);
#7286=ORIENTED_EDGE('',*,*,#5422,.F.);
#7287=ORIENTED_EDGE('',*,*,#5421,.T.);
#7288=ORIENTED_EDGE('',*,*,#5423,.T.);
#7289=ORIENTED_EDGE('',*,*,#5424,.F.);
#7290=ORIENTED_EDGE('',*,*,#5425,.F.);
#7291=ORIENTED_EDGE('',*,*,#5426,.T.);
#7292=ORIENTED_EDGE('',*,*,#5427,.T.);
#7293=ORIENTED_EDGE('',*,*,#5428,.T.);
#7294=ORIENTED_EDGE('',*,*,#5424,.T.);
#7295=ORIENTED_EDGE('',*,*,#5429,.T.);
#7296=ORIENTED_EDGE('',*,*,#5426,.F.);
#7297=ORIENTED_EDGE('',*,*,#5423,.F.);
#7298=ORIENTED_EDGE('',*,*,#5420,.T.);
#7299=ORIENTED_EDGE('',*,*,#5430,.F.);
#7300=ORIENTED_EDGE('',*,*,#5431,.F.);
#7301=ORIENTED_EDGE('',*,*,#5432,.T.);
#7302=ORIENTED_EDGE('',*,*,#5433,.F.);
#7303=ORIENTED_EDGE('',*,*,#5434,.T.);
#7304=ORIENTED_EDGE('',*,*,#5435,.T.);
#7305=ORIENTED_EDGE('',*,*,#5436,.T.);
#7306=ORIENTED_EDGE('',*,*,#5437,.T.);
#7307=ORIENTED_EDGE('',*,*,#5438,.T.);
#7308=ORIENTED_EDGE('',*,*,#5427,.F.);
#7309=ORIENTED_EDGE('',*,*,#5436,.F.);
#7310=ORIENTED_EDGE('',*,*,#5439,.F.);
#7311=ORIENTED_EDGE('',*,*,#5440,.F.);
#7312=ORIENTED_EDGE('',*,*,#5437,.F.);
#7313=ORIENTED_EDGE('',*,*,#5435,.F.);
#7314=ORIENTED_EDGE('',*,*,#5428,.F.);
#7315=ORIENTED_EDGE('',*,*,#5438,.F.);
#7316=ORIENTED_EDGE('',*,*,#5440,.T.);
#7317=ORIENTED_EDGE('',*,*,#5441,.F.);
#7318=ORIENTED_EDGE('',*,*,#5442,.F.);
#7319=ORIENTED_EDGE('',*,*,#5443,.T.);
#7320=ORIENTED_EDGE('',*,*,#5444,.F.);
#7321=ORIENTED_EDGE('',*,*,#5445,.T.);
#7322=ORIENTED_EDGE('',*,*,#5422,.T.);
#7323=ORIENTED_EDGE('',*,*,#5425,.T.);
#7324=ORIENTED_EDGE('',*,*,#5439,.T.);
#7325=ORIENTED_EDGE('',*,*,#5434,.F.);
#7326=ORIENTED_EDGE('',*,*,#5446,.F.);
#7327=ORIENTED_EDGE('',*,*,#5441,.T.);
#7328=ORIENTED_EDGE('',*,*,#5442,.T.);
#7329=ORIENTED_EDGE('',*,*,#5446,.T.);
#7330=ORIENTED_EDGE('',*,*,#5433,.T.);
#7331=ORIENTED_EDGE('',*,*,#5447,.T.);
#7332=ORIENTED_EDGE('',*,*,#5448,.T.);
#7333=ORIENTED_EDGE('',*,*,#5449,.T.);
#7334=ORIENTED_EDGE('',*,*,#5448,.F.);
#7335=ORIENTED_EDGE('',*,*,#5450,.F.);
#7336=ORIENTED_EDGE('',*,*,#5451,.T.);
#7337=ORIENTED_EDGE('',*,*,#5429,.F.);
#7338=ORIENTED_EDGE('',*,*,#5451,.F.);
#7339=ORIENTED_EDGE('',*,*,#5452,.F.);
#7340=ORIENTED_EDGE('',*,*,#5453,.F.);
#7341=ORIENTED_EDGE('',*,*,#5454,.F.);
#7342=ORIENTED_EDGE('',*,*,#5447,.F.);
#7343=ORIENTED_EDGE('',*,*,#5432,.F.);
#7344=ORIENTED_EDGE('',*,*,#5455,.F.);
#7345=ORIENTED_EDGE('',*,*,#5452,.T.);
#7346=ORIENTED_EDGE('',*,*,#5450,.T.);
#7347=ORIENTED_EDGE('',*,*,#5449,.F.);
#7348=ORIENTED_EDGE('',*,*,#5454,.T.);
#7349=ORIENTED_EDGE('',*,*,#5456,.F.);
#7350=ORIENTED_EDGE('',*,*,#5443,.F.);
#7351=ORIENTED_EDGE('',*,*,#5431,.T.);
#7352=ORIENTED_EDGE('',*,*,#5457,.T.);
#7353=ORIENTED_EDGE('',*,*,#5444,.T.);
#7354=ORIENTED_EDGE('',*,*,#5456,.T.);
#7355=ORIENTED_EDGE('',*,*,#5453,.T.);
#7356=ORIENTED_EDGE('',*,*,#5455,.T.);
#7357=ORIENTED_EDGE('',*,*,#5419,.T.);
#7358=ORIENTED_EDGE('',*,*,#5445,.F.);
#7359=ORIENTED_EDGE('',*,*,#5457,.F.);
#7360=ORIENTED_EDGE('',*,*,#5430,.T.);
#8104=CYLINDRICAL_SURFACE('',#9288,0.2117);
#8411=ADVANCED_FACE('',(#1117),#712,.F.);
#8412=ADVANCED_FACE('',(#1118),#713,.T.);
#8413=ADVANCED_FACE('',(#1119,#436),#714,.T.);
#8414=ADVANCED_FACE('',(#1120),#715,.T.);
#8415=ADVANCED_FACE('',(#1121),#716,.T.);
#8416=ADVANCED_FACE('',(#1122),#717,.F.);
#8417=ADVANCED_FACE('',(#1123),#718,.T.);
#8418=ADVANCED_FACE('',(#1124),#719,.T.);
#8419=ADVANCED_FACE('',(#1125),#720,.T.);
#8420=ADVANCED_FACE('',(#1126),#8104,.F.);
#8421=ADVANCED_FACE('',(#1127),#721,.F.);
#8422=ADVANCED_FACE('',(#1128),#722,.F.);
#8423=ADVANCED_FACE('',(#1129),#723,.T.);
#8424=ADVANCED_FACE('',(#1130),#724,.T.);
#8601=CLOSED_SHELL('',(#8411,#8412,#8413,#8414,#8415,#8416,#8417,#8418,
#8419,#8420,#8421,#8422,#8423,#8424));
#9276=AXIS2_PLACEMENT_3D('',#13512,#11004,#11005);
#9277=AXIS2_PLACEMENT_3D('',#13513,#11006,#11007);
#9278=AXIS2_PLACEMENT_3D('',#13522,#11012,#11013);
#9279=AXIS2_PLACEMENT_3D('',#13528,#11017,#11018);
#9280=AXIS2_PLACEMENT_3D('',#13535,#11022,#11023);
#9281=AXIS2_PLACEMENT_3D('',#13536,#11024,#11025);
#9282=AXIS2_PLACEMENT_3D('',#13550,#11033,#11034);
#9283=AXIS2_PLACEMENT_3D('',#13554,#11037,#11038);
#9284=AXIS2_PLACEMENT_3D('',#13558,#11041,#11042);
#9285=AXIS2_PLACEMENT_3D('',#13568,#11048,#11049);
#9286=AXIS2_PLACEMENT_3D('',#13570,#11051,#11052);
#9287=AXIS2_PLACEMENT_3D('',#13574,#11054,#11055);
#9288=AXIS2_PLACEMENT_3D('',#13576,#11057,#11058);
#9289=AXIS2_PLACEMENT_3D('',#13578,#11059,#11060);
#9290=AXIS2_PLACEMENT_3D('',#13581,#11062,#11063);
#9291=AXIS2_PLACEMENT_3D('',#13583,#11064,#11065);
#9292=AXIS2_PLACEMENT_3D('',#13584,#11066,#11067);
#9293=AXIS2_PLACEMENT_3D('',#13585,#11068,#11069);
#9294=AXIS2_PLACEMENT_3D('',#13587,#11071,#11072);
#9295=AXIS2_PLACEMENT_3D('',#13589,#11074,#11075);
#9296=AXIS2_PLACEMENT_3D('',#13591,#11077,#11078);
#11004=DIRECTION('axis',(0.,0.,1.));
#11005=DIRECTION('refdir',(1.,0.,0.));
#11006=DIRECTION('center_axis',(0.,0.,1.));
#11007=DIRECTION('ref_axis',(1.,0.,0.));
#11008=DIRECTION('',(1.,0.,0.));
#11009=DIRECTION('',(0.,-1.,0.));
#11010=DIRECTION('',(-1.,0.,0.));
#11011=DIRECTION('',(0.,1.,0.));
#11012=DIRECTION('center_axis',(0.,1.,0.));
#11013=DIRECTION('ref_axis',(-1.,0.,0.));
#11014=DIRECTION('',(0.,0.,1.));
#11015=DIRECTION('',(-1.,0.,0.));
#11016=DIRECTION('',(0.,0.,1.));
#11017=DIRECTION('center_axis',(0.,0.,1.));
#11018=DIRECTION('ref_axis',(1.,0.,0.));
#11019=DIRECTION('',(0.,-1.,0.));
#11020=DIRECTION('',(1.,0.,0.));
#11021=DIRECTION('',(0.,1.,0.));
#11022=DIRECTION('center_axis',(0.,0.,-1.));
#11023=DIRECTION('ref_axis',(1.,0.,0.));
#11024=DIRECTION('center_axis',(-1.,0.,0.));
#11025=DIRECTION('ref_axis',(0.,-1.,0.));
#11026=DIRECTION('',(0.,0.,1.));
#11027=DIRECTION('',(0.,0.707106781186548,0.707106781186548));
#11028=DIRECTION('',(0.,-1.,0.));
#11029=DIRECTION('',(0.,0.707106781186548,-0.707106781186548));
#11030=DIRECTION('',(0.,0.,1.));
#11031=DIRECTION('',(0.,-1.,0.));
#11032=DIRECTION('',(0.,0.,1.));
#11033=DIRECTION('center_axis',(0.,-1.,0.));
#11034=DIRECTION('ref_axis',(1.,0.,0.));
#11035=DIRECTION('',(1.,0.,0.));
#11036=DIRECTION('',(0.,0.,1.));
#11037=DIRECTION('center_axis',(0.,0.,1.));
#11038=DIRECTION('ref_axis',(1.,0.,0.));
#11039=DIRECTION('',(-1.,0.,0.));
#11040=DIRECTION('',(0.,1.,0.));
#11041=DIRECTION('center_axis',(1.,0.,0.));
#11042=DIRECTION('ref_axis',(0.,1.,0.));
#11043=DIRECTION('',(0.,0.,1.));
#11044=DIRECTION('',(0.,-0.707106781186548,0.707106781186548));
#11045=DIRECTION('',(0.,1.,0.));
#11046=DIRECTION('',(0.,-0.707106781186548,-0.707106781186548));
#11047=DIRECTION('',(0.,0.,1.));
#11048=DIRECTION('center_axis',(0.,-1.,0.));
#11049=DIRECTION('ref_axis',(1.,0.,0.));
#11050=DIRECTION('',(-1.,0.,0.));
#11051=DIRECTION('center_axis',(0.,-0.707106781186548,-0.707106781186548));
#11052=DIRECTION('ref_axis',(-1.,0.,0.));
#11053=DIRECTION('',(1.,0.,0.));
#11054=DIRECTION('center_axis',(0.,0.707106781186548,0.707106781186548));
#11055=DIRECTION('ref_axis',(0.,0.707106781186547,-0.707106781186547));
#11056=DIRECTION('',(1.,0.,0.));
#11057=DIRECTION('center_axis',(0.,0.,1.));
#11058=DIRECTION('ref_axis',(1.,0.,0.));
#11059=DIRECTION('center_axis',(0.,0.,-1.));
#11060=DIRECTION('ref_axis',(1.,0.,0.));
#11061=DIRECTION('',(0.,0.,1.));
#11062=DIRECTION('center_axis',(0.,0.,-1.));
#11063=DIRECTION('ref_axis',(1.,0.,0.));
#11064=DIRECTION('center_axis',(0.,-0.707106781186548,0.707106781186548));
#11065=DIRECTION('ref_axis',(0.,0.707106781186547,0.707106781186547));
#11066=DIRECTION('center_axis',(0.,0.,-1.));
#11067=DIRECTION('ref_axis',(1.,0.,0.));
#11068=DIRECTION('center_axis',(0.,0.,1.));
#11069=DIRECTION('ref_axis',(1.,0.,0.));
#11070=DIRECTION('',(-1.,0.,0.));
#11071=DIRECTION('center_axis',(0.,0.,1.));
#11072=DIRECTION('ref_axis',(1.,0.,0.));
#11073=DIRECTION('',(-1.,0.,0.));
#11074=DIRECTION('center_axis',(0.,0.707106781186548,-0.707106781186548));
#11075=DIRECTION('ref_axis',(-1.,0.,0.));
#11076=DIRECTION('',(1.,0.,0.));
#11077=DIRECTION('center_axis',(0.,1.,0.));
#11078=DIRECTION('ref_axis',(-1.,0.,0.));
#13512=CARTESIAN_POINT('',(0.,0.,0.));
#13513=CARTESIAN_POINT('Origin',(0.,0.395,0.25));
#13514=CARTESIAN_POINT('',(-0.5,0.3,0.25));
#13515=CARTESIAN_POINT('',(0.5,0.3,0.25));
#13516=CARTESIAN_POINT('',(0.25,0.3,0.25));
#13517=CARTESIAN_POINT('',(-0.5,0.5,0.25));
#13518=CARTESIAN_POINT('',(-0.5,0.5,0.25));
#13519=CARTESIAN_POINT('',(0.5,0.5,0.25));
#13520=CARTESIAN_POINT('',(0.5,0.5,0.25));
#13521=CARTESIAN_POINT('',(0.5,0.29,0.25));
#13522=CARTESIAN_POINT('Origin',(0.5,0.5,0.25));
#13523=CARTESIAN_POINT('',(-0.5,0.5,0.4));
#13524=CARTESIAN_POINT('',(-0.5,0.5,0.25));
#13525=CARTESIAN_POINT('',(0.5,0.5,0.4));
#13526=CARTESIAN_POINT('',(0.5,0.5,0.4));
#13527=CARTESIAN_POINT('',(0.5,0.5,0.25));
#13528=CARTESIAN_POINT('Origin',(0.,0.,0.4));
#13529=CARTESIAN_POINT('',(-0.5,-0.5,0.4));
#13530=CARTESIAN_POINT('',(-0.5,0.5,0.4));
#13531=CARTESIAN_POINT('',(0.5,-0.5,0.4));
#13532=CARTESIAN_POINT('',(-0.5,-0.5,0.4));
#13533=CARTESIAN_POINT('',(0.5,-0.3,0.4));
#13534=CARTESIAN_POINT('',(-0.2117,2.59257727379495E-17,0.4));
#13535=CARTESIAN_POINT('Origin',(0.,0.,0.4));
#13536=CARTESIAN_POINT('Origin',(-0.5,0.3,0.));
#13537=CARTESIAN_POINT('',(-0.5,0.3,0.15));
#13538=CARTESIAN_POINT('',(-0.5,0.3,0.));
#13539=CARTESIAN_POINT('',(-0.5,0.15,0.));
#13540=CARTESIAN_POINT('',(-0.5,0.225,0.075));
#13541=CARTESIAN_POINT('',(-0.5,-0.15,0.));
#13542=CARTESIAN_POINT('',(-0.5,0.3,0.));
#13543=CARTESIAN_POINT('',(-0.5,-0.3,0.15));
#13544=CARTESIAN_POINT('',(-0.5,-0.075,-0.075));
#13545=CARTESIAN_POINT('',(-0.5,-0.3,0.25));
#13546=CARTESIAN_POINT('',(-0.5,-0.3,0.));
#13547=CARTESIAN_POINT('',(-0.5,-0.5,0.25));
#13548=CARTESIAN_POINT('',(-0.5,-0.29,0.25));
#13549=CARTESIAN_POINT('',(-0.5,-0.5,0.25));
#13550=CARTESIAN_POINT('Origin',(-0.5,-0.5,0.25));
#13551=CARTESIAN_POINT('',(0.5,-0.5,0.25));
#13552=CARTESIAN_POINT('',(-0.5,-0.5,0.25));
#13553=CARTESIAN_POINT('',(0.5,-0.5,0.25));
#13554=CARTESIAN_POINT('Origin',(0.,-0.395,0.25));
#13555=CARTESIAN_POINT('',(0.5,-0.3,0.25));
#13556=CARTESIAN_POINT('',(-0.25,-0.3,0.25));
#13557=CARTESIAN_POINT('',(0.5,-0.5,0.25));
#13558=CARTESIAN_POINT('Origin',(0.5,-0.3,0.));
#13559=CARTESIAN_POINT('',(0.5,-0.3,0.15));
#13560=CARTESIAN_POINT('',(0.5,-0.3,0.));
#13561=CARTESIAN_POINT('',(0.5,-0.15,0.));
#13562=CARTESIAN_POINT('',(0.5,-0.225,0.075));
#13563=CARTESIAN_POINT('',(0.5,0.15,0.));
#13564=CARTESIAN_POINT('',(0.5,-0.3,0.));
#13565=CARTESIAN_POINT('',(0.5,0.3,0.15));
#13566=CARTESIAN_POINT('',(0.5,0.075,-0.075));
#13567=CARTESIAN_POINT('',(0.5,0.3,0.));
#13568=CARTESIAN_POINT('Origin',(-0.5,-0.3,0.));
#13569=CARTESIAN_POINT('',(-0.25,-0.3,0.15));
#13570=CARTESIAN_POINT('Origin',(-0.25,-0.225,0.075));
#13571=CARTESIAN_POINT('',(-0.149388386429468,-0.15,0.));
#13572=CARTESIAN_POINT('',(-0.25,-0.15,0.));
#13573=CARTESIAN_POINT('',(0.149388386429468,-0.15,0.));
#13574=CARTESIAN_POINT('Origin',(0.,0.,-0.15));
#13575=CARTESIAN_POINT('',(-0.25,-0.15,0.));
#13576=CARTESIAN_POINT('Origin',(0.,0.,-0.1));
#13577=CARTESIAN_POINT('',(-0.2117,-2.59257727379495E-17,0.));
#13578=CARTESIAN_POINT('Origin',(0.,0.,0.));
#13579=CARTESIAN_POINT('',(-0.2117,-2.59257727379495E-17,-0.1));
#13580=CARTESIAN_POINT('',(-0.149388386429468,0.15,0.));
#13581=CARTESIAN_POINT('Origin',(0.,0.,0.));
#13582=CARTESIAN_POINT('',(0.149388386429468,0.15,0.));
#13583=CARTESIAN_POINT('Origin',(0.,0.,-0.15));
#13584=CARTESIAN_POINT('Origin',(0.,0.,0.));
#13585=CARTESIAN_POINT('Origin',(0.,0.,0.));
#13586=CARTESIAN_POINT('',(0.25,0.15,0.));
#13587=CARTESIAN_POINT('Origin',(0.,0.,0.));
#13588=CARTESIAN_POINT('',(0.25,0.15,0.));
#13589=CARTESIAN_POINT('Origin',(0.25,0.225,0.075));
#13590=CARTESIAN_POINT('',(0.25,0.3,0.15));
#13591=CARTESIAN_POINT('Origin',(0.5,0.3,0.));
#14429=UNCERTAINTY_MEASURE_WITH_UNIT(LENGTH_MEASURE(0.001),#14479,
'DISTANCE_ACCURACY_VALUE',
'Maximum model space distance between geometric entities at asserted c
onnectivities');
#14446=UNCERTAINTY_MEASURE_WITH_UNIT(LENGTH_MEASURE(0.001),#14479,
'DISTANCE_ACCURACY_VALUE',
'Maximum model space distance between geometric entities at asserted c
onnectivities');
#14461=(
GEOMETRIC_REPRESENTATION_CONTEXT(3)
GLOBAL_UNCERTAINTY_ASSIGNED_CONTEXT((#14429))
GLOBAL_UNIT_ASSIGNED_CONTEXT((#14479,#14481,#14482))
REPRESENTATION_CONTEXT('','3D')
);
#14478=(
GEOMETRIC_REPRESENTATION_CONTEXT(3)
GLOBAL_UNCERTAINTY_ASSIGNED_CONTEXT((#14446))
GLOBAL_UNIT_ASSIGNED_CONTEXT((#14479,#14481,#14482))
REPRESENTATION_CONTEXT('','3D')
);
#14479=(
LENGTH_UNIT()
NAMED_UNIT(*)
SI_UNIT(.CENTI.,.METRE.)
);
#14481=(
NAMED_UNIT(*)
PLANE_ANGLE_UNIT()
SI_UNIT($,.RADIAN.)
);
#14482=(
NAMED_UNIT(*)
SI_UNIT($,.STERADIAN.)
SOLID_ANGLE_UNIT()
);
#14497=SHAPE_DEFINITION_REPRESENTATION(#14528,#14617);
#14528=PRODUCT_DEFINITION_SHAPE('',$,#14649);
#14617=SHAPE_REPRESENTATION('',(#9276),#14461);
#14634=PRODUCT_DEFINITION_CONTEXT('part definition',#14729,'design');
#14649=PRODUCT_DEFINITION('Captive slot nut','Captive slot nut',#14680,
#14634);
#14680=PRODUCT_DEFINITION_FORMATION('',$,#14745);
#14729=APPLICATION_CONTEXT(
'Core Data for Automotive Mechanical Design Process');
#14730=PRODUCT_CONTEXT('part definition',#14729,'mechanical');
#14745=PRODUCT('Captive slot nut','Captive slot nut','Captive slot nut',
(#14730));
#14832=COLOUR_RGB('Black',0.12,0.14,0.17);
#14833=FILL_AREA_STYLE_COLOUR('',#14832);
#14834=FILL_AREA_STYLE('',(#14833));
#14835=SURFACE_STYLE_FILL_AREA(#14834);
#14836=SURFACE_SIDE_STYLE('',(#14835));
#14837=SURFACE_STYLE_USAGE(.BOTH.,#14836);
#14838=PRESENTATION_STYLE_ASSIGNMENT((#14837));
ENDSEC;
END-ISO-10303-21;
